ISO-10303-21;
HEADER;
/* Generated by software containing ST-Developer
 * from STEP Tools, Inc. (www.steptools.com) 
 */

FILE_DESCRIPTION(
/* description */ ('Belt tensioner idler arm'),
/* implementation_level */ '2;1');

FILE_NAME(
/* name */ 'Cap Screw - M4x16.step',
/* time_stamp */ '2026-10-28T03:22:15-07:00',
/* author */ (''),
/* organization */ (''),
/* preprocessor_version */ 'ST-DEVELOPER v20.2',
/* originating_system */ 'Autodesk Translation Framework v15.17.0.0',
/* authorisation */ '');

FILE_SCHEMA (('AUTOMOTIVE_DESIGN { 1 0 10303 214 3 1 1 }'));
ENDSEC;

DATA;
#10=MECHANICAL_DESIGN_GEOMETRIC_PRESENTATION_REPRESENTATION('',(#458),#12779);
#286=ORIENTED_CLOSED_SHELL('',*,#6194,.F.);
#290=BREP_WITH_VOIDS('Body1',#6193,(#286));
#300=CONICAL_SURFACE('',#6785,0.325,0.785398163397448);
#301=CONICAL_SURFACE('',#6789,0.335,0.785398163397448);
#302=CONICAL_SURFACE('',#6793,0.21,0.463647609000806);
#303=CONICAL_SURFACE('',#6797,0.18,0.785398163397448);
#390=SHAPE_REPRESENTATION_RELATIONSHIP('SRR','None',#12936,#424);
#424=ADVANCED_BREP_SHAPE_REPRESENTATION('',(#290),#12753);
#458=STYLED_ITEM('',(#13191),#290);
#561=FACE_BOUND('',#1345,.T.);
#729=PLANE('',#6783);
#730=PLANE('',#6791);
#731=PLANE('',#6799);
#732=PLANE('',#6800);
#733=PLANE('',#6801);
#734=PLANE('',#6802);
#735=PLANE('',#6803);
#736=PLANE('',#6804);
#737=PLANE('',#6805);
#738=PLANE('',#6806);
#739=PLANE('',#6807);
#939=FACE_OUTER_BOUND('',#1340,.T.);
#940=FACE_OUTER_BOUND('',#1341,.T.);
#941=FACE_OUTER_BOUND('',#1342,.T.);
#942=FACE_OUTER_BOUND('',#1343,.T.);
#943=FACE_OUTER_BOUND('',#1344,.T.);
#944=FACE_OUTER_BOUND('',#1346,.T.);
#945=FACE_OUTER_BOUND('',#1347,.T.);
#946=FACE_OUTER_BOUND('',#1348,.T.);
#947=FACE_OUTER_BOUND('',#1349,.T.);
#948=FACE_OUTER_BOUND('',#1350,.T.);
#949=FACE_OUTER_BOUND('',#1351,.T.);
#950=FACE_OUTER_BOUND('',#1352,.T.);
#951=FACE_OUTER_BOUND('',#1353,.T.);
#952=FACE_OUTER_BOUND('',#1354,.T.);
#953=FACE_OUTER_BOUND('',#1355,.T.);
#954=FACE_OUTER_BOUND('',#1356,.T.);
#955=FACE_OUTER_BOUND('',#1357,.T.);
#1340=EDGE_LOOP('',(#4490));
#1341=EDGE_LOOP('',(#4491,#4492,#4493,#4494));
#1342=EDGE_LOOP('',(#4495,#4496,#4497,#4498));
#1343=EDGE_LOOP('',(#4499,#4500,#4501,#4502));
#1344=EDGE_LOOP('',(#4503));
#1345=EDGE_LOOP('',(#4504));
#1346=EDGE_LOOP('',(#4505,#4506,#4507,#4508));
#1347=EDGE_LOOP('',(#4509,#4510,#4511,#4512));
#1348=EDGE_LOOP('',(#4513,#4514,#4515,#4516));
#1349=EDGE_LOOP('',(#4517));
#1350=EDGE_LOOP('',(#4518,#4519,#4520,#4521));
#1351=EDGE_LOOP('',(#4522,#4523,#4524,#4525));
#1352=EDGE_LOOP('',(#4526,#4527,#4528,#4529));
#1353=EDGE_LOOP('',(#4530,#4531,#4532,#4533));
#1354=EDGE_LOOP('',(#4534,#4535,#4536,#4537));
#1355=EDGE_LOOP('',(#4538,#4539,#4540,#4541));
#1356=EDGE_LOOP('',(#4542,#4543,#4544,#4545,#4546,#4547));
#1357=EDGE_LOOP('',(#4548,#4549,#4550,#4551,#4552,#4553));
#1819=LINE('',#10624,#2168);
#1820=LINE('',#10628,#2169);
#1821=LINE('',#10632,#2170);
#1822=LINE('',#10639,#2171);
#1823=LINE('',#10643,#2172);
#1824=LINE('',#10647,#2173);
#1825=LINE('',#10652,#2174);
#1826=LINE('',#10654,#2175);
#1827=LINE('',#10656,#2176);
#1828=LINE('',#10657,#2177);
#1829=LINE('',#10660,#2178);
#1830=LINE('',#10662,#2179);
#1831=LINE('',#10663,#2180);
#1832=LINE('',#10666,#2181);
#1833=LINE('',#10668,#2182);
#1834=LINE('',#10669,#2183);
#1835=LINE('',#10672,#2184);
#1836=LINE('',#10674,#2185);
#1837=LINE('',#10675,#2186);
#1838=LINE('',#10678,#2187);
#1839=LINE('',#10680,#2188);
#1840=LINE('',#10681,#2189);
#1841=LINE('',#10683,#2190);
#1842=LINE('',#10684,#2191);
#2168=VECTOR('',#7915,0.325);
#2169=VECTOR('',#7920,0.35);
#2170=VECTOR('',#7925,0.335);
#2171=VECTOR('',#7934,0.21);
#2172=VECTOR('',#7939,0.2);
#2173=VECTOR('',#7944,0.18);
#2174=VECTOR('',#7949,1.);
#2175=VECTOR('',#7950,1.);
#2176=VECTOR('',#7951,1.);
#2177=VECTOR('',#7952,1.);
#2178=VECTOR('',#7955,1.);
#2179=VECTOR('',#7956,1.);
#2180=VECTOR('',#7957,1.);
#2181=VECTOR('',#7960,1.);
#2182=VECTOR('',#7961,1.);
#2183=VECTOR('',#7962,1.);
#2184=VECTOR('',#7965,1.);
#2185=VECTOR('',#7966,1.);
#2186=VECTOR('',#7967,1.);
#2187=VECTOR('',#7970,1.);
#2188=VECTOR('',#7971,1.);
#2189=VECTOR('',#7972,1.);
#2190=VECTOR('',#7975,1.);
#2191=VECTOR('',#7976,1.);
#2470=CIRCLE('',#6784,0.3);
#2471=CIRCLE('',#6786,0.35);
#2472=CIRCLE('',#6788,0.35);
#2473=CIRCLE('',#6790,0.32);
#2474=CIRCLE('',#6792,0.22);
#2475=CIRCLE('',#6794,0.1954);
#2476=CIRCLE('',#6796,0.1954);
#2477=CIRCLE('',#6798,0.16);
#2899=VERTEX_POINT('',#10619);
#2900=VERTEX_POINT('',#10622);
#2901=VERTEX_POINT('',#10626);
#2902=VERTEX_POINT('',#10630);
#2903=VERTEX_POINT('',#10634);
#2904=VERTEX_POINT('',#10637);
#2905=VERTEX_POINT('',#10641);
#2906=VERTEX_POINT('',#10645);
#2907=VERTEX_POINT('',#10650);
#2908=VERTEX_POINT('',#10651);
#2909=VERTEX_POINT('',#10653);
#2910=VERTEX_POINT('',#10655);
#2911=VERTEX_POINT('',#10659);
#2912=VERTEX_POINT('',#10661);
#2913=VERTEX_POINT('',#10665);
#2914=VERTEX_POINT('',#10667);
#2915=VERTEX_POINT('',#10671);
#2916=VERTEX_POINT('',#10673);
#2917=VERTEX_POINT('',#10677);
#2918=VERTEX_POINT('',#10679);
#3500=EDGE_CURVE('',#2899,#2899,#2470,.T.);
#3501=EDGE_CURVE('',#2900,#2900,#2471,.T.);
#3502=EDGE_CURVE('',#2900,#2899,#1819,.T.);
#3503=EDGE_CURVE('',#2901,#2901,#2472,.T.);
#3504=EDGE_CURVE('',#2901,#2900,#1820,.T.);
#3505=EDGE_CURVE('',#2902,#2902,#2473,.T.);
#3506=EDGE_CURVE('',#2902,#2901,#1821,.T.);
#3507=EDGE_CURVE('',#2903,#2903,#2474,.T.);
#3508=EDGE_CURVE('',#2904,#2904,#2475,.F.);
#3509=EDGE_CURVE('',#2904,#2903,#1822,.T.);
#3510=EDGE_CURVE('',#2905,#2905,#2476,.F.);
#3511=EDGE_CURVE('',#2905,#2904,#1823,.T.);
#3512=EDGE_CURVE('',#2906,#2906,#2477,.T.);
#3513=EDGE_CURVE('',#2906,#2905,#1824,.T.);
#3514=EDGE_CURVE('',#2907,#2908,#1825,.T.);
#3515=EDGE_CURVE('',#2908,#2909,#1826,.T.);
#3516=EDGE_CURVE('',#2909,#2910,#1827,.T.);
#3517=EDGE_CURVE('',#2907,#2910,#1828,.T.);
#3518=EDGE_CURVE('',#2908,#2911,#1829,.T.);
#3519=EDGE_CURVE('',#2911,#2912,#1830,.T.);
#3520=EDGE_CURVE('',#2912,#2909,#1831,.T.);
#3521=EDGE_CURVE('',#2911,#2913,#1832,.T.);
#3522=EDGE_CURVE('',#2913,#2914,#1833,.T.);
#3523=EDGE_CURVE('',#2914,#2912,#1834,.T.);
#3524=EDGE_CURVE('',#2913,#2915,#1835,.T.);
#3525=EDGE_CURVE('',#2915,#2916,#1836,.T.);
#3526=EDGE_CURVE('',#2916,#2914,#1837,.T.);
#3527=EDGE_CURVE('',#2915,#2917,#1838,.T.);
#3528=EDGE_CURVE('',#2917,#2918,#1839,.T.);
#3529=EDGE_CURVE('',#2918,#2916,#1840,.T.);
#3530=EDGE_CURVE('',#2917,#2907,#1841,.T.);
#3531=EDGE_CURVE('',#2910,#2918,#1842,.T.);
#4490=ORIENTED_EDGE('',*,*,#3500,.F.);
#4491=ORIENTED_EDGE('',*,*,#3501,.F.);
#4492=ORIENTED_EDGE('',*,*,#3502,.T.);
#4493=ORIENTED_EDGE('',*,*,#3500,.T.);
#4494=ORIENTED_EDGE('',*,*,#3502,.F.);
#4495=ORIENTED_EDGE('',*,*,#3503,.F.);
#4496=ORIENTED_EDGE('',*,*,#3504,.T.);
#4497=ORIENTED_EDGE('',*,*,#3501,.T.);
#4498=ORIENTED_EDGE('',*,*,#3504,.F.);
#4499=ORIENTED_EDGE('',*,*,#3505,.F.);
#4500=ORIENTED_EDGE('',*,*,#3506,.T.);
#4501=ORIENTED_EDGE('',*,*,#3503,.T.);
#4502=ORIENTED_EDGE('',*,*,#3506,.F.);
#4503=ORIENTED_EDGE('',*,*,#3505,.T.);
#4504=ORIENTED_EDGE('',*,*,#3507,.F.);
#4505=ORIENTED_EDGE('',*,*,#3508,.F.);
#4506=ORIENTED_EDGE('',*,*,#3509,.T.);
#4507=ORIENTED_EDGE('',*,*,#3507,.T.);
#4508=ORIENTED_EDGE('',*,*,#3509,.F.);
#4509=ORIENTED_EDGE('',*,*,#3510,.F.);
#4510=ORIENTED_EDGE('',*,*,#3511,.T.);
#4511=ORIENTED_EDGE('',*,*,#3508,.T.);
#4512=ORIENTED_EDGE('',*,*,#3511,.F.);
#4513=ORIENTED_EDGE('',*,*,#3512,.F.);
#4514=ORIENTED_EDGE('',*,*,#3513,.T.);
#4515=ORIENTED_EDGE('',*,*,#3510,.T.);
#4516=ORIENTED_EDGE('',*,*,#3513,.F.);
#4517=ORIENTED_EDGE('',*,*,#3512,.T.);
#4518=ORIENTED_EDGE('',*,*,#3514,.T.);
#4519=ORIENTED_EDGE('',*,*,#3515,.T.);
#4520=ORIENTED_EDGE('',*,*,#3516,.T.);
#4521=ORIENTED_EDGE('',*,*,#3517,.F.);
#4522=ORIENTED_EDGE('',*,*,#3518,.T.);
#4523=ORIENTED_EDGE('',*,*,#3519,.T.);
#4524=ORIENTED_EDGE('',*,*,#3520,.T.);
#4525=ORIENTED_EDGE('',*,*,#3515,.F.);
#4526=ORIENTED_EDGE('',*,*,#3521,.T.);
#4527=ORIENTED_EDGE('',*,*,#3522,.T.);
#4528=ORIENTED_EDGE('',*,*,#3523,.T.);
#4529=ORIENTED_EDGE('',*,*,#3519,.F.);
#4530=ORIENTED_EDGE('',*,*,#3524,.T.);
#4531=ORIENTED_EDGE('',*,*,#3525,.T.);
#4532=ORIENTED_EDGE('',*,*,#3526,.T.);
#4533=ORIENTED_EDGE('',*,*,#3522,.F.);
#4534=ORIENTED_EDGE('',*,*,#3527,.T.);
#4535=ORIENTED_EDGE('',*,*,#3528,.T.);
#4536=ORIENTED_EDGE('',*,*,#3529,.T.);
#4537=ORIENTED_EDGE('',*,*,#3525,.F.);
#4538=ORIENTED_EDGE('',*,*,#3530,.T.);
#4539=ORIENTED_EDGE('',*,*,#3517,.T.);
#4540=ORIENTED_EDGE('',*,*,#3531,.T.);
#4541=ORIENTED_EDGE('',*,*,#3528,.F.);
#4542=ORIENTED_EDGE('',*,*,#3530,.F.);
#4543=ORIENTED_EDGE('',*,*,#3527,.F.);
#4544=ORIENTED_EDGE('',*,*,#3524,.F.);
#4545=ORIENTED_EDGE('',*,*,#3521,.F.);
#4546=ORIENTED_EDGE('',*,*,#3518,.F.);
#4547=ORIENTED_EDGE('',*,*,#3514,.F.);
#4548=ORIENTED_EDGE('',*,*,#3531,.F.);
#4549=ORIENTED_EDGE('',*,*,#3516,.F.);
#4550=ORIENTED_EDGE('',*,*,#3520,.F.);
#4551=ORIENTED_EDGE('',*,*,#3523,.F.);
#4552=ORIENTED_EDGE('',*,*,#3526,.F.);
#4553=ORIENTED_EDGE('',*,*,#3529,.F.);
#5690=CYLINDRICAL_SURFACE('',#6787,0.35);
#5691=CYLINDRICAL_SURFACE('',#6795,0.1954);
#5916=ADVANCED_FACE('',(#939),#729,.T.);
#5917=ADVANCED_FACE('',(#940),#300,.T.);
#5918=ADVANCED_FACE('',(#941),#5690,.T.);
#5919=ADVANCED_FACE('',(#942),#301,.T.);
#5920=ADVANCED_FACE('',(#943,#561),#730,.T.);
#5921=ADVANCED_FACE('',(#944),#302,.T.);
#5922=ADVANCED_FACE('',(#945),#5691,.T.);
#5923=ADVANCED_FACE('',(#946),#303,.T.);
#5924=ADVANCED_FACE('',(#947),#731,.T.);
#5925=ADVANCED_FACE('',(#948),#732,.F.);
#5926=ADVANCED_FACE('',(#949),#733,.F.);
#5927=ADVANCED_FACE('',(#950),#734,.F.);
#5928=ADVANCED_FACE('',(#951),#735,.F.);
#5929=ADVANCED_FACE('',(#952),#736,.F.);
#5930=ADVANCED_FACE('',(#953),#737,.F.);
#5931=ADVANCED_FACE('',(#954),#738,.F.);
#5932=ADVANCED_FACE('',(#955),#739,.F.);
#6193=CLOSED_SHELL('',(#5916,#5917,#5918,#5919,#5920,#5921,#5922,#5923,
#5924));
#6194=CLOSED_SHELL('',(#5925,#5926,#5927,#5928,#5929,#5930,#5931,#5932));
#6782=AXIS2_PLACEMENT_3D('',#10617,#7905,#7906);
#6783=AXIS2_PLACEMENT_3D('',#10618,#7907,#7908);
#6784=AXIS2_PLACEMENT_3D('',#10620,#7909,#7910);
#6785=AXIS2_PLACEMENT_3D('',#10621,#7911,#7912);
#6786=AXIS2_PLACEMENT_3D('',#10623,#7913,#7914);
#6787=AXIS2_PLACEMENT_3D('',#10625,#7916,#7917);
#6788=AXIS2_PLACEMENT_3D('',#10627,#7918,#7919);
#6789=AXIS2_PLACEMENT_3D('',#10629,#7921,#7922);
#6790=AXIS2_PLACEMENT_3D('',#10631,#7923,#7924);
#6791=AXIS2_PLACEMENT_3D('',#10633,#7926,#7927);
#6792=AXIS2_PLACEMENT_3D('',#10635,#7928,#7929);
#6793=AXIS2_PLACEMENT_3D('',#10636,#7930,#7931);
#6794=AXIS2_PLACEMENT_3D('',#10638,#7932,#7933);
#6795=AXIS2_PLACEMENT_3D('',#10640,#7935,#7936);
#6796=AXIS2_PLACEMENT_3D('',#10642,#7937,#7938);
#6797=AXIS2_PLACEMENT_3D('',#10644,#7940,#7941);
#6798=AXIS2_PLACEMENT_3D('',#10646,#7942,#7943);
#6799=AXIS2_PLACEMENT_3D('',#10648,#7945,#7946);
#6800=AXIS2_PLACEMENT_3D('',#10649,#7947,#7948);
#6801=AXIS2_PLACEMENT_3D('',#10658,#7953,#7954);
#6802=AXIS2_PLACEMENT_3D('',#10664,#7958,#7959);
#6803=AXIS2_PLACEMENT_3D('',#10670,#7963,#7964);
#6804=AXIS2_PLACEMENT_3D('',#10676,#7968,#7969);
#6805=AXIS2_PLACEMENT_3D('',#10682,#7973,#7974);
#6806=AXIS2_PLACEMENT_3D('',#10685,#7977,#7978);
#6807=AXIS2_PLACEMENT_3D('',#10686,#7979,#7980);
#7905=DIRECTION('axis',(0.,0.,1.));
#7906=DIRECTION('refdir',(1.,0.,0.));
#7907=DIRECTION('center_axis',(0.,1.,0.));
#7908=DIRECTION('ref_axis',(0.,0.,1.));
#7909=DIRECTION('center_axis',(0.,-1.,0.));
#7910=DIRECTION('ref_axis',(1.,0.,0.));
#7911=DIRECTION('center_axis',(0.,-1.,0.));
#7912=DIRECTION('ref_axis',(1.,0.,0.));
#7913=DIRECTION('center_axis',(0.,-1.,0.));
#7914=DIRECTION('ref_axis',(1.,0.,0.));
#7915=DIRECTION('',(0.707106781186547,0.707106781186548,8.65956056235493E-17));
#7916=DIRECTION('center_axis',(0.,-1.,0.));
#7917=DIRECTION('ref_axis',(1.,0.,0.));
#7918=DIRECTION('center_axis',(0.,-1.,0.));
#7919=DIRECTION('ref_axis',(1.,0.,0.));
#7920=DIRECTION('',(0.,1.,0.));
#7921=DIRECTION('center_axis',(0.,1.,0.));
#7922=DIRECTION('ref_axis',(1.,0.,0.));
#7923=DIRECTION('center_axis',(0.,-1.,0.));
#7924=DIRECTION('ref_axis',(1.,0.,0.));
#7925=DIRECTION('',(-0.707106781186547,0.707106781186548,-8.65956056235493E-17));
#7926=DIRECTION('center_axis',(0.,-1.,0.));
#7927=DIRECTION('ref_axis',(0.,0.,-1.));
#7928=DIRECTION('center_axis',(0.,-1.,0.));
#7929=DIRECTION('ref_axis',(1.,0.,0.));
#7930=DIRECTION('center_axis',(0.,1.,0.));
#7931=DIRECTION('ref_axis',(1.,0.,0.));
#7932=DIRECTION('center_axis',(0.,1.,0.));
#7933=DIRECTION('ref_axis',(1.,0.,0.));
#7934=DIRECTION('',(-0.447213595499958,0.894427190999916,-5.47678698264203E-17));
#7935=DIRECTION('center_axis',(0.,-1.,0.));
#7936=DIRECTION('ref_axis',(1.,0.,0.));
#7937=DIRECTION('center_axis',(0.,1.,0.));
#7938=DIRECTION('ref_axis',(1.,0.,0.));
#7939=DIRECTION('',(0.,1.,0.));
#7940=DIRECTION('center_axis',(0.,1.,0.));
#7941=DIRECTION('ref_axis',(1.,0.,0.));
#7942=DIRECTION('center_axis',(0.,-1.,0.));
#7943=DIRECTION('ref_axis',(1.,0.,0.));
#7944=DIRECTION('',(-0.707106781186547,0.707106781186548,-8.65956056235493E-17));
#7945=DIRECTION('center_axis',(0.,-1.,0.));
#7946=DIRECTION('ref_axis',(0.,0.,-1.));
#7947=DIRECTION('center_axis',(0.866025403784439,0.,-0.5));
#7948=DIRECTION('ref_axis',(0.5,0.,0.866025403784439));
#7949=DIRECTION('',(-0.5,0.,-0.866025403784439));
#7950=DIRECTION('',(0.,-1.,0.));
#7951=DIRECTION('',(0.5,0.,0.866025403784439));
#7952=DIRECTION('',(0.,-1.,0.));
#7953=DIRECTION('center_axis',(1.60246890531964E-16,0.,-1.));
#7954=DIRECTION('ref_axis',(1.,0.,1.60246890531964E-16));
#7955=DIRECTION('',(-1.,0.,-1.60246890531964E-16));
#7956=DIRECTION('',(0.,-1.,0.));
#7957=DIRECTION('',(1.,0.,1.60246890531964E-16));
#7958=DIRECTION('center_axis',(-0.866025403784439,0.,-0.5));
#7959=DIRECTION('ref_axis',(0.5,0.,-0.866025403784439));
#7960=DIRECTION('',(-0.5,0.,0.866025403784439));
#7961=DIRECTION('',(0.,-1.,0.));
#7962=DIRECTION('',(0.5,0.,-0.866025403784439));
#7963=DIRECTION('center_axis',(-0.866025403784439,0.,0.5));
#7964=DIRECTION('ref_axis',(-0.5,0.,-0.866025403784439));
#7965=DIRECTION('',(0.5,0.,0.866025403784439));
#7966=DIRECTION('',(0.,-1.,0.));
#7967=DIRECTION('',(-0.5,0.,-0.866025403784439));
#7968=DIRECTION('center_axis',(-1.60246890531964E-16,0.,1.));
#7969=DIRECTION('ref_axis',(-1.,0.,-1.60246890531964E-16));
#7970=DIRECTION('',(1.,0.,1.60246890531964E-16));
#7971=DIRECTION('',(0.,-1.,0.));
#7972=DIRECTION('',(-1.,0.,-1.60246890531964E-16));
#7973=DIRECTION('center_axis',(0.866025403784439,0.,0.5));
#7974=DIRECTION('ref_axis',(-0.5,0.,0.866025403784439));
#7975=DIRECTION('',(0.5,0.,-0.866025403784439));
#7976=DIRECTION('',(-0.5,0.,0.866025403784439));
#7977=DIRECTION('center_axis',(0.,1.,0.));
#7978=DIRECTION('ref_axis',(1.,0.,0.));
#7979=DIRECTION('center_axis',(0.,-1.,0.));
#7980=DIRECTION('ref_axis',(0.,0.,-1.));
#10617=CARTESIAN_POINT('',(0.,0.,0.));
#10618=CARTESIAN_POINT('Origin',(0.3,0.4,0.));
#10619=CARTESIAN_POINT('',(-0.3,0.4,-3.67394039744206E-17));
#10620=CARTESIAN_POINT('Origin',(0.,0.4,0.));
#10621=CARTESIAN_POINT('Origin',(0.,0.375,0.));
#10622=CARTESIAN_POINT('',(-0.35,0.35,-4.28626379701573E-17));
#10623=CARTESIAN_POINT('Origin',(0.,0.35,0.));
#10624=CARTESIAN_POINT('',(-0.325,0.375,-3.9801020972289E-17));
#10625=CARTESIAN_POINT('Origin',(0.,0.19,0.));
#10626=CARTESIAN_POINT('',(-0.35,0.03,-4.28626379701574E-17));
#10627=CARTESIAN_POINT('Origin',(0.,0.03,0.));
#10628=CARTESIAN_POINT('',(-0.35,0.19,-4.28626379701574E-17));
#10629=CARTESIAN_POINT('Origin',(0.,0.0149999999999999,0.));
#10630=CARTESIAN_POINT('',(-0.32,-3.29597460435593E-17,-3.91886975727153E-17));
#10631=CARTESIAN_POINT('Origin',(0.,0.,0.));
#10632=CARTESIAN_POINT('',(-0.335,0.0149999999999999,-4.10256677714363E-17));
#10633=CARTESIAN_POINT('Origin',(0.22,0.,0.));
#10634=CARTESIAN_POINT('',(-0.22,-6.93889390390723E-18,-2.69422295812418E-17));
#10635=CARTESIAN_POINT('Origin',(0.,0.,0.));
#10636=CARTESIAN_POINT('Origin',(0.,-0.02,0.));
#10637=CARTESIAN_POINT('',(-0.1954,-0.0492,2.39295984553393E-17));
#10638=CARTESIAN_POINT('Origin',(0.,-0.0492,0.));
#10639=CARTESIAN_POINT('',(-0.21,-0.02,-2.57175827820944E-17));
#10640=CARTESIAN_POINT('Origin',(0.,-0.8,0.));
#10641=CARTESIAN_POINT('',(-0.1954,-1.5646,2.39295984553393E-17));
#10642=CARTESIAN_POINT('Origin',(0.,-1.5646,0.));
#10643=CARTESIAN_POINT('',(-0.1954,-0.8,-2.39295984553393E-17));
#10644=CARTESIAN_POINT('Origin',(0.,-1.58,0.));
#10645=CARTESIAN_POINT('',(-0.16,-1.6,-1.95943487863577E-17));
#10646=CARTESIAN_POINT('Origin',(0.,-1.6,0.));
#10647=CARTESIAN_POINT('',(-0.18,-1.58,-2.20436423846524E-17));
#10648=CARTESIAN_POINT('Origin',(0.,-1.6,0.));
#10649=CARTESIAN_POINT('Origin',(0.0866025403784439,-0.4,-0.15));
#10650=CARTESIAN_POINT('',(0.173205080756888,-0.4,0.));
#10651=CARTESIAN_POINT('',(0.0866025403784439,-0.4,-0.15));
#10652=CARTESIAN_POINT('',(0.173205080756888,-0.4,0.));
#10653=CARTESIAN_POINT('',(0.0866025403784439,-0.64,-0.15));
#10654=CARTESIAN_POINT('',(0.0866025403784439,-0.4,-0.15));
#10655=CARTESIAN_POINT('',(0.173205080756888,-0.64,0.));
#10656=CARTESIAN_POINT('',(0.173205080756888,-0.64,0.));
#10657=CARTESIAN_POINT('',(0.173205080756888,-0.4,0.));
#10658=CARTESIAN_POINT('Origin',(-0.0866025403784438,-0.4,-0.15));
#10659=CARTESIAN_POINT('',(-0.0866025403784438,-0.4,-0.15));
#10660=CARTESIAN_POINT('',(0.0866025403784439,-0.4,-0.15));
#10661=CARTESIAN_POINT('',(-0.0866025403784438,-0.64,-0.15));
#10662=CARTESIAN_POINT('',(-0.0866025403784438,-0.4,-0.15));
#10663=CARTESIAN_POINT('',(0.0866025403784439,-0.64,-0.15));
#10664=CARTESIAN_POINT('Origin',(-0.173205080756888,-0.4,-2.77555756156289E-17));
#10665=CARTESIAN_POINT('',(-0.173205080756888,-0.4,-2.12115047744981E-17));
#10666=CARTESIAN_POINT('',(-0.0866025403784438,-0.4,-0.15));
#10667=CARTESIAN_POINT('',(-0.173205080756888,-0.64,-2.77555756156289E-17));
#10668=CARTESIAN_POINT('',(-0.173205080756888,-0.4,-2.12115047744981E-17));
#10669=CARTESIAN_POINT('',(-0.0866025403784438,-0.64,-0.15));
#10670=CARTESIAN_POINT('Origin',(-0.0866025403784439,-0.4,0.15));
#10671=CARTESIAN_POINT('',(-0.0866025403784439,-0.4,0.15));
#10672=CARTESIAN_POINT('',(-0.173205080756888,-0.4,-2.12115047744981E-17));
#10673=CARTESIAN_POINT('',(-0.0866025403784439,-0.64,0.15));
#10674=CARTESIAN_POINT('',(-0.0866025403784439,-0.4,0.15));
#10675=CARTESIAN_POINT('',(-0.173205080756888,-0.64,-2.12115047744981E-17));
#10676=CARTESIAN_POINT('Origin',(0.0866025403784439,-0.4,0.15));
#10677=CARTESIAN_POINT('',(0.0866025403784439,-0.4,0.15));
#10678=CARTESIAN_POINT('',(-0.0866025403784439,-0.4,0.15));
#10679=CARTESIAN_POINT('',(0.0866025403784439,-0.64,0.15));
#10680=CARTESIAN_POINT('',(0.0866025403784439,-0.4,0.15));
#10681=CARTESIAN_POINT('',(-0.0866025403784439,-0.64,0.15));
#10682=CARTESIAN_POINT('Origin',(0.173205080756888,-0.4,0.));
#10683=CARTESIAN_POINT('',(0.0866025403784439,-0.4,0.15));
#10684=CARTESIAN_POINT('',(0.0866025403784439,-0.64,0.15));
#10685=CARTESIAN_POINT('Origin',(0.,-0.4,-2.77555756156289E-17));
#10686=CARTESIAN_POINT('Origin',(0.,-0.64,-2.77555756156289E-17));
#12713=UNCERTAINTY_MEASURE_WITH_UNIT(LENGTH_MEASURE(0.001),#12780,
'DISTANCE_ACCURACY_VALUE',
'Maximum model space distance between geometric entities at asserted c
onnectivities');
#12739=UNCERTAINTY_MEASURE_WITH_UNIT(LENGTH_MEASURE(0.001),#12780,
'DISTANCE_ACCURACY_VALUE',
'Maximum model space distance between geometric entities at asserted c
onnectivities');
#12753=(
GEOMETRIC_REPRESENTATION_CONTEXT(3)
GLOBAL_UNCERTAINTY_ASSIGNED_CONTEXT((#12713))
GLOBAL_UNIT_ASSIGNED_CONTEXT((#12780,#12782,#12783))
REPRESENTATION_CONTEXT('','3D')
);
#12779=(
GEOMETRIC_REPRESENTATION_CONTEXT(3)
GLOBAL_UNCERTAINTY_ASSIGNED_CONTEXT((#12739))
GLOBAL_UNIT_ASSIGNED_CONTEXT((#12780,#12782,#12783))
REPRESENTATION_CONTEXT('','3D')
);
#12780=(
LENGTH_UNIT()
NAMED_UNIT(*)
SI_UNIT(.CENTI.,.METRE.)
);
#12782=(
NAMED_UNIT(*)
PLANE_ANGLE_UNIT()
SI_UNIT($,.RADIAN.)
);
#12783=(
NAMED_UNIT(*)
SI_UNIT($,.STERADIAN.)
SOLID_ANGLE_UNIT()
);
#12797=SHAPE_DEFINITION_REPRESENTATION(#12836,#12936);
#12836=PRODUCT_DEFINITION_SHAPE('',$,#12976);
#12936=SHAPE_REPRESENTATION('',(#6782),#12753);
#12962=PRODUCT_DEFINITION_CONTEXT('part definition',#13081,'design');
#12976=PRODUCT_DEFINITION('Cap Screw - M4x16','Cap Screw - M4x16',#13015,
#12962);
#13015=PRODUCT_DEFINITION_FORMATION('',$,#13096);
#13081=APPLICATION_CONTEXT(
'Core Data for Automotive Mechanical Design Process');
#13082=PRODUCT_CONTEXT('part definition',#13081,'mechanical');
#13096=PRODUCT('Cap Screw - M4x16','Cap Screw - M4x16',
'Cap Screw - M4x16',(#13082));
#13185=COLOUR_RGB('Black',0.12,0.14,0.17);
#13186=FILL_AREA_STYLE_COLOUR('',#13185);
#13187=FILL_AREA_STYLE('',(#13186));
#13188=SURFACE_STYLE_FILL_AREA(#13187);
#13189=SURFACE_SIDE_STYLE('',(#13188));
#13190=SURFACE_STYLE_USAGE(.BOTH.,#13189);
#13191=PRESENTATION_STYLE_ASSIGNMENT((#13190));
ENDSEC;
END-ISO-10303-21;
